ISO-10303-21;
HEADER;
/* Generated by software containing ST-Developer
 * from STEP Tools, Inc. (www.steptools.com) 
 */

FILE_DESCRIPTION(
/* description */ ('Drill jig with bushing plate'),
/* implementation_level */ '2;1');

FILE_NAME(
/* name */ 'Drill bushing 10 (1).step',
/* time_stamp */ '2026-10-27T10:51:08-07:00',
/* author */ (''),
/* organization */ (''),
/* preprocessor_version */ 'ST-DEVELOPER v20.2',
/* originating_system */ 'Autodesk Translation Framework v15.17.0.0',
/* authorisation */ '');

FILE_SCHEMA (('AUTOMOTIVE_DESIGN { 1 0 10303 214 3 1 1 }'));
ENDSEC;

DATA;
#10=MECHANICAL_DESIGN_GEOMETRIC_PRESENTATION_REPRESENTATION('',(#244),#6638);
#196=SHAPE_REPRESENTATION_RELATIONSHIP('SRR','None',#6761,#220);
#220=ADVANCED_BREP_SHAPE_REPRESENTATION('',(#266),#6634);
#244=STYLED_ITEM('',(#6929),#266);
#266=MANIFOLD_SOLID_BREP('Body1',#3613);
#364=FACE_BOUND('',#1007,.T.);
#365=FACE_BOUND('',#1010,.T.);
#366=FACE_BOUND('',#1014,.T.);
#490=PLANE('',#4284);
#491=PLANE('',#4289);
#492=PLANE('',#4295);
#697=FACE_OUTER_BOUND('',#1006,.T.);
#698=FACE_OUTER_BOUND('',#1008,.T.);
#699=FACE_OUTER_BOUND('',#1009,.T.);
#700=FACE_OUTER_BOUND('',#1011,.T.);
#701=FACE_OUTER_BOUND('',#1012,.T.);
#702=FACE_OUTER_BOUND('',#1013,.T.);
#1006=EDGE_LOOP('',(#3239));
#1007=EDGE_LOOP('',(#3240));
#1008=EDGE_LOOP('',(#3241,#3242,#3243,#3244));
#1009=EDGE_LOOP('',(#3245));
#1010=EDGE_LOOP('',(#3246));
#1011=EDGE_LOOP('',(#3247,#3248,#3249,#3250));
#1012=EDGE_LOOP('',(#3251,#3252,#3253,#3254));
#1013=EDGE_LOOP('',(#3255));
#1014=EDGE_LOOP('',(#3256));
#1275=LINE('',#6508,#1536);
#1276=LINE('',#6514,#1537);
#1277=LINE('',#6518,#1538);
#1536=VECTOR('',#5390,0.9);
#1537=VECTOR('',#5397,0.5);
#1538=VECTOR('',#5402,0.7);
#1706=CIRCLE('',#4285,0.9);
#1707=CIRCLE('',#4286,0.7);
#1708=CIRCLE('',#4288,0.9);
#1709=CIRCLE('',#4290,0.5);
#1710=CIRCLE('',#4292,0.5);
#1711=CIRCLE('',#4294,0.7);
#1986=VERTEX_POINT('',#6501);
#1987=VERTEX_POINT('',#6503);
#1988=VERTEX_POINT('',#6506);
#1989=VERTEX_POINT('',#6510);
#1990=VERTEX_POINT('',#6513);
#1991=VERTEX_POINT('',#6517);
#2407=EDGE_CURVE('',#1986,#1986,#1706,.T.);
#2408=EDGE_CURVE('',#1987,#1987,#1707,.T.);
#2409=EDGE_CURVE('',#1988,#1988,#1708,.T.);
#2410=EDGE_CURVE('',#1988,#1986,#1275,.T.);
#2411=EDGE_CURVE('',#1989,#1989,#1709,.T.);
#2412=EDGE_CURVE('',#1989,#1990,#1276,.T.);
#2413=EDGE_CURVE('',#1990,#1990,#1710,.T.);
#2414=EDGE_CURVE('',#1987,#1991,#1277,.T.);
#2415=EDGE_CURVE('',#1991,#1991,#1711,.T.);
#3239=ORIENTED_EDGE('',*,*,#2407,.F.);
#3240=ORIENTED_EDGE('',*,*,#2408,.T.);
#3241=ORIENTED_EDGE('',*,*,#2409,.F.);
#3242=ORIENTED_EDGE('',*,*,#2410,.T.);
#3243=ORIENTED_EDGE('',*,*,#2407,.T.);
#3244=ORIENTED_EDGE('',*,*,#2410,.F.);
#3245=ORIENTED_EDGE('',*,*,#2409,.T.);
#3246=ORIENTED_EDGE('',*,*,#2411,.T.);
#3247=ORIENTED_EDGE('',*,*,#2411,.F.);
#3248=ORIENTED_EDGE('',*,*,#2412,.T.);
#3249=ORIENTED_EDGE('',*,*,#2413,.T.);
#3250=ORIENTED_EDGE('',*,*,#2412,.F.);
#3251=ORIENTED_EDGE('',*,*,#2408,.F.);
#3252=ORIENTED_EDGE('',*,*,#2414,.T.);
#3253=ORIENTED_EDGE('',*,*,#2415,.T.);
#3254=ORIENTED_EDGE('',*,*,#2414,.F.);
#3255=ORIENTED_EDGE('',*,*,#2415,.F.);
#3256=ORIENTED_EDGE('',*,*,#2413,.F.);
#3369=CYLINDRICAL_SURFACE('',#4287,0.9);
#3370=CYLINDRICAL_SURFACE('',#4291,0.5);
#3371=CYLINDRICAL_SURFACE('',#4293,0.7);
#3572=ADVANCED_FACE('',(#697,#364),#490,.F.);
#3573=ADVANCED_FACE('',(#698),#3369,.T.);
#3574=ADVANCED_FACE('',(#699,#365),#491,.T.);
#3575=ADVANCED_FACE('',(#700),#3370,.F.);
#3576=ADVANCED_FACE('',(#701),#3371,.T.);
#3577=ADVANCED_FACE('',(#702,#366),#492,.F.);
#3613=CLOSED_SHELL('',(#3572,#3573,#3574,#3575,#3576,#3577));
#4283=AXIS2_PLACEMENT_3D('',#6499,#5378,#5379);
#4284=AXIS2_PLACEMENT_3D('',#6500,#5380,#5381);
#4285=AXIS2_PLACEMENT_3D('',#6502,#5382,#5383);
#4286=AXIS2_PLACEMENT_3D('',#6504,#5384,#5385);
#4287=AXIS2_PLACEMENT_3D('',#6505,#5386,#5387);
#4288=AXIS2_PLACEMENT_3D('',#6507,#5388,#5389);
#4289=AXIS2_PLACEMENT_3D('',#6509,#5391,#5392);
#4290=AXIS2_PLACEMENT_3D('',#6511,#5393,#5394);
#4291=AXIS2_PLACEMENT_3D('',#6512,#5395,#5396);
#4292=AXIS2_PLACEMENT_3D('',#6515,#5398,#5399);
#4293=AXIS2_PLACEMENT_3D('',#6516,#5400,#5401);
#4294=AXIS2_PLACEMENT_3D('',#6519,#5403,#5404);
#4295=AXIS2_PLACEMENT_3D('',#6520,#5405,#5406);
#5378=DIRECTION('axis',(0.,0.,1.));
#5379=DIRECTION('refdir',(1.,0.,0.));
#5380=DIRECTION('center_axis',(0.,0.,1.));
#5381=DIRECTION('ref_axis',(1.,0.,0.));
#5382=DIRECTION('center_axis',(0.,0.,1.));
#5383=DIRECTION('ref_axis',(1.,0.,0.));
#5384=DIRECTION('center_axis',(0.,0.,1.));
#5385=DIRECTION('ref_axis',(1.,0.,0.));
#5386=DIRECTION('center_axis',(0.,0.,1.));
#5387=DIRECTION('ref_axis',(1.,0.,0.));
#5388=DIRECTION('center_axis',(0.,0.,1.));
#5389=DIRECTION('ref_axis',(1.,0.,0.));
#5390=DIRECTION('',(0.,0.,-1.));
#5391=DIRECTION('center_axis',(0.,0.,1.));
#5392=DIRECTION('ref_axis',(1.,0.,0.));
#5393=DIRECTION('center_axis',(0.,0.,-1.));
#5394=DIRECTION('ref_axis',(1.,0.,0.));
#5395=DIRECTION('center_axis',(0.,0.,1.));
#5396=DIRECTION('ref_axis',(1.,0.,0.));
#5397=DIRECTION('',(0.,0.,-1.));
#5398=DIRECTION('center_axis',(0.,0.,-1.));
#5399=DIRECTION('ref_axis',(1.,0.,0.));
#5400=DIRECTION('center_axis',(0.,0.,1.));
#5401=DIRECTION('ref_axis',(1.,0.,0.));
#5402=DIRECTION('',(0.,0.,-1.));
#5403=DIRECTION('center_axis',(0.,0.,1.));
#5404=DIRECTION('ref_axis',(1.,0.,0.));
#5405=DIRECTION('center_axis',(0.,0.,1.));
#5406=DIRECTION('ref_axis',(1.,0.,0.));
#6499=CARTESIAN_POINT('',(0.,0.,0.));
#6500=CARTESIAN_POINT('Origin',(2.,1.,4.5));
#6501=CARTESIAN_POINT('',(1.1,1.,4.5));
#6502=CARTESIAN_POINT('Origin',(2.,1.,4.5));
#6503=CARTESIAN_POINT('',(1.3,1.,4.5));
#6504=CARTESIAN_POINT('Origin',(2.,1.,4.5));
#6505=CARTESIAN_POINT('Origin',(2.,1.,4.5));
#6506=CARTESIAN_POINT('',(1.1,1.,4.7));
#6507=CARTESIAN_POINT('Origin',(2.,1.,4.7));
#6508=CARTESIAN_POINT('',(1.1,1.,4.5));
#6509=CARTESIAN_POINT('Origin',(2.,1.,4.7));
#6510=CARTESIAN_POINT('',(1.5,1.,4.7));
#6511=CARTESIAN_POINT('Origin',(2.,1.,4.7));
#6512=CARTESIAN_POINT('Origin',(2.,1.,2.5));
#6513=CARTESIAN_POINT('',(1.5,1.,2.5));
#6514=CARTESIAN_POINT('',(1.5,1.,2.5));
#6515=CARTESIAN_POINT('Origin',(2.,1.,2.5));
#6516=CARTESIAN_POINT('Origin',(2.,1.,2.5));
#6517=CARTESIAN_POINT('',(1.3,1.,2.5));
#6518=CARTESIAN_POINT('',(1.3,1.,2.5));
#6519=CARTESIAN_POINT('Origin',(2.,1.,2.5));
#6520=CARTESIAN_POINT('Origin',(2.,1.,2.5));
#6605=UNCERTAINTY_MEASURE_WITH_UNIT(LENGTH_MEASURE(0.001),#6639,
'DISTANCE_ACCURACY_VALUE',
'Maximum model space distance between geometric entities at asserted c
onnectivities');
#6609=UNCERTAINTY_MEASURE_WITH_UNIT(LENGTH_MEASURE(0.001),#6639,
'DISTANCE_ACCURACY_VALUE',
'Maximum model space distance between geometric entities at asserted c
onnectivities');
#6634=(
GEOMETRIC_REPRESENTATION_CONTEXT(3)
GLOBAL_UNCERTAINTY_ASSIGNED_CONTEXT((#6605))
GLOBAL_UNIT_ASSIGNED_CONTEXT((#6639,#6641,#6642))
REPRESENTATION_CONTEXT('','3D')
);
#6638=(
GEOMETRIC_REPRESENTATION_CONTEXT(3)
GLOBAL_UNCERTAINTY_ASSIGNED_CONTEXT((#6609))
GLOBAL_UNIT_ASSIGNED_CONTEXT((#6639,#6641,#6642))
REPRESENTATION_CONTEXT('','3D')
);
#6639=(
LENGTH_UNIT()
NAMED_UNIT(*)
SI_UNIT(.CENTI.,.METRE.)
);
#6641=(
NAMED_UNIT(*)
PLANE_ANGLE_UNIT()
SI_UNIT($,.RADIAN.)
);
#6642=(
NAMED_UNIT(*)
SI_UNIT($,.STERADIAN.)
SOLID_ANGLE_UNIT()
);
#6667=SHAPE_DEFINITION_REPRESENTATION(#6723,#6761);
#6723=PRODUCT_DEFINITION_SHAPE('',$,#6790);
#6761=SHAPE_REPRESENTATION('',(#4283),#6634);
#6765=PRODUCT_DEFINITION_CONTEXT('part definition',#6851,'design');
#6790=PRODUCT_DEFINITION('Drill bushing 10 (1)','Drill bushing 10 (1)',#6818,
#6765);
#6818=PRODUCT_DEFINITION_FORMATION('',$,#6877);
#6851=APPLICATION_CONTEXT(
'Core Data for Automotive Mechanical Design Process');
#6852=PRODUCT_CONTEXT('part definition',#6851,'mechanical');
#6877=PRODUCT('Drill bushing 10 (1)','Drill bushing 10 (1)',
'Drill bushing 10 (1)',(#6852));
#6923=COLOUR_RGB('Light Blue',0.38,0.62,0.78);
#6924=FILL_AREA_STYLE_COLOUR('',#6923);
#6925=FILL_AREA_STYLE('',(#6924));
#6926=SURFACE_STYLE_FILL_AREA(#6925);
#6927=SURFACE_SIDE_STYLE('',(#6926));
#6928=SURFACE_STYLE_USAGE(.BOTH.,#6927);
#6929=PRESENTATION_STYLE_ASSIGNMENT((#6928));
ENDSEC;
END-ISO-10303-21;
